ISO-10303-21;
HEADER;
FILE_DESCRIPTION (('STEP AP214'),
    '1' );
FILE_NAME ('Roller 1.step',
    '2026-10-26T17:37:43',
    ( '' ),
    ( '' ),
    'SwSTEP 2.0',
    'SolidWorks 2024',
    '' );
FILE_SCHEMA (( 'AUTOMOTIVE_DESIGN' ));
ENDSEC;

DATA;
#36=DIRECTION ( 'NONE',  ( 0.000000000000000000, 0.000000000000000000, -1.000000000000000000 ) ) ;
#107=ORIENTED_EDGE ( 'NONE', *, *, #21741, .F. ) ;
#384=ADVANCED_FACE ( 'NONE', ( #14318 ), #1776, .F. ) ;
#404=EDGE_CURVE ( 'NONE', #2635, #21912, #17488, .T. ) ;
#497=CARTESIAN_POINT ( 'NONE',  ( 138.7804567094461561, -3576.796478203516017, 2257.629402114759159 ) ) ;
#530=ADVANCED_FACE ( 'NONE', ( #9101 ), #16243, .F. ) ;
#619=DIRECTION ( 'NONE',  ( -1.000000000000000000, 0.000000000000000000, 0.000000000000000000 ) ) ;
#721=AXIS2_PLACEMENT_3D ( 'NONE', #17891, #3471, #10623 ) ;
#741=PRODUCT_DEFINITION_FORMATION_WITH_SPECIFIED_SOURCE ( 'ANY', '', #20975, .NOT_KNOWN. ) ;
#828=CARTESIAN_POINT ( 'NONE',  ( 137.4277150837954196, -3577.744018727676121, 2257.824198891456490 ) ) ;
#858=CARTESIAN_POINT ( 'NONE',  ( 140.0740604329243979, -3582.321215597040464, 2257.597438756844895 ) ) ;
#903=CARTESIAN_POINT ( 'NONE',  ( 141.8426865414658664, -3577.614611570635589, 2257.800363196316084 ) ) ;
#906=DIRECTION ( 'NONE',  ( 1.000000000000000000, 0.000000000000000000, 0.000000000000000000 ) ) ;
#917=EDGE_LOOP ( 'NONE', ( #19607, #7311 ) ) ;
#920=CARTESIAN_POINT ( 'NONE',  ( 141.1265829792455975, -3661.973233856808747, 2257.683488261172442 ) ) ;
#978=CARTESIAN_POINT ( 'NONE',  ( 141.5805787415576162, -3581.637520105196927, 2257.752117343301052 ) ) ;
#1022=CARTESIAN_POINT ( 'NONE',  ( 140.6228164679936867, -3656.807677064647578, 2257.629692242904184 ) ) ;
#1055=CARTESIAN_POINT ( 'NONE',  ( 137.4378581446332532, -3581.229941748726105, 2257.824813627034928 ) ) ;
#1084=ORIENTED_EDGE ( 'NONE', *, *, #8969, .F. ) ;
#1131=B_SPLINE_CURVE_WITH_KNOTS ( 'NONE', 3,
 ( #7869, #8105, #7758, #18748, #9623, #15249, #4573, #11716, #18869, #4118, #18411, #2814, #22148, #11264, #18640, #14790, #21928, #11489 ),
 .UNSPECIFIED., .F., .F.,
 ( 4, 2, 2, 2, 2, 2, 2, 2, 4 ),
 ( 0.008925482226561637714, 0.009483346987770943301, 0.01004121174898024715, 0.01059907651018955274, 0.01115694127139885833, 0.01171480603260816218, 0.01227267079381746777, 0.01283053555502677162, 0.01338840031623607721 ),
 .UNSPECIFIED. ) ;
#1140=CARTESIAN_POINT ( 'NONE',  ( 142.2556445848496480, -3578.231573646348352, 2257.890254708840530 ) ) ;
#1228=ADVANCED_FACE ( 'NONE', ( #3414 ), #15843, .T. ) ;
#1273=ORIENTED_EDGE ( 'NONE', *, *, #7526, .T. ) ;
#1381=CARTESIAN_POINT ( 'NONE',  ( 140.4431196414874989, -3576.742565540147552, 2257.615983594398131 ) ) ;
#1587=DIRECTION ( 'NONE',  ( 0.000000000000000000, -1.000000000000000000, 0.000000000000000000 ) ) ;
#1634=DIRECTION ( 'NONE',  ( 0.000000000000000000, 0.000000000000000000, -1.000000000000000000 ) ) ;
#1708=CARTESIAN_POINT ( 'NONE',  ( 142.5447999999989861, -3579.494999999999891, 2272.030000000000200 ) ) ;
#1739=CARTESIAN_POINT ( 'NONE',  ( 139.6999999999999886, -3576.650200000000950, 2257.592639999999847 ) ) ;
#1776=PLANE ( 'NONE',  #9856 ) ;
#1820=ORIENTED_EDGE ( 'NONE', *, *, #18113, .F. ) ;
#1932=EDGE_CURVE ( 'NONE', #21382, #14294, #18786, .T. ) ;
#1993=APPLICATION_CONTEXT ( 'configuration controlled 3d designs of mechanical parts and assemblies' ) ;
#1994=ADVANCED_FACE ( 'NONE', ( #13443 ), #5859, .F. ) ;
#2222=ORIENTED_EDGE ( 'NONE', *, *, #20139, .T. ) ;
#2257=( GEOMETRIC_REPRESENTATION_CONTEXT ( 3 ) GLOBAL_UNCERTAINTY_ASSIGNED_CONTEXT ( ( #16741 ) ) GLOBAL_UNIT_ASSIGNED_CONTEXT ( ( #21126, #3419, #23094 ) ) REPRESENTATION_CONTEXT ( 'NONE', 'WORKASPACE' ) );
#2259=CARTESIAN_POINT ( 'NONE',  ( 136.8552000000009912, -3579.494999999999891, 2257.962944264955695 ) ) ;
#2299=DIRECTION ( 'NONE',  ( 1.000000000000000000, 0.000000000000000000, 0.000000000000000000 ) ) ;
#2353=CARTESIAN_POINT ( 'NONE',  ( 140.0740604339752622, -3662.331215596936545, 2257.597438756872180 ) ) ;
#2409=DIRECTION ( 'NONE',  ( 0.000000000000000000, -1.000000000000000000, 0.000000000000000000 ) ) ;
#2468=CARTESIAN_POINT ( 'NONE',  ( 142.4524393066650703, -3660.248099168110912, 2257.938841367611076 ) ) ;
#2494=VECTOR ( 'NONE', #8399, 1000.000000000000000 ) ;
#2606=CARTESIAN_POINT ( 'NONE',  ( 0.000000000000000000, 0.000000000000000000, 0.000000000000000000 ) ) ;
#2622=CARTESIAN_POINT ( 'NONE',  ( 142.1839422240020951, -3580.930228203060778, 2257.872821503999148 ) ) ;
#2635=VERTEX_POINT ( 'NONE', #16417 ) ;
#2683=CARTESIAN_POINT ( 'NONE',  ( 139.6999999999999886, -3570.287499999999909, 2268.705139999999574 ) ) ;
#2781=CARTESIAN_POINT ( 'NONE',  ( 140.0750197480601287, -3656.678786553412920, 2257.597441013359457 ) ) ;
#2787=EDGE_CURVE ( 'NONE', #17996, #18205, #15241, .T. ) ;
#2793=ORIENTED_EDGE ( 'NONE', *, *, #14881, .T. ) ;
#2804=AXIS2_PLACEMENT_3D ( 'NONE', #14806, #4587, #619 ) ;
#2814=CARTESIAN_POINT ( 'NONE',  ( 138.2712681005278057, -3661.972087661942624, 2257.683753147038260 ) ) ;
#2900=ORIENTED_EDGE ( 'NONE', *, *, #9181, .T. ) ;
#2909=CARTESIAN_POINT ( 'NONE',  ( 142.5262150965213550, -3579.120943345095384, 2257.957974173306866 ) ) ;
#2927=PRODUCT_DEFINITION_CONTEXT ( 'detailed design', #7699, 'design' ) ;
#2936=CARTESIAN_POINT ( 'NONE',  ( 138.9568795186264936, -3582.247434258886642, 2257.615983644609059 ) ) ;
#2945=ORIENTED_EDGE ( 'NONE', *, *, #7414, .F. ) ;
#3011=ORIENTED_EDGE ( 'NONE', *, *, #404, .T. ) ;
#3062=DIRECTION ( 'NONE',  ( 0.000000000000000000, -1.000000000000000000, 0.000000000000000000 ) ) ;
#3063=B_SPLINE_CURVE_WITH_KNOTS ( 'NONE', 3,
 ( #13408, #18453, #858, #20440, #6275, #4389, #4497, #18338, #978, #14836, #2622, #9767, #15170, #5935, #11631, #18789 ),
 .UNSPECIFIED., .F., .F.,
 ( 4, 2, 2, 2, 2, 2, 2, 4 ),
 ( 0.000000000000000000, 0.0005578396384567584597, 0.001115679276913516919, 0.001673518915370275162, 0.002231358553827033839, 0.003347037830739731101, 0.003904877469195421405, 0.004462717107651111709 ),
 .UNSPECIFIED. ) ;
#3138=CARTESIAN_POINT ( 'NONE',  ( 142.1683190434573305, -3578.068567422205888, 2257.869726352968428 ) ) ;
#3260=CARTESIAN_POINT ( 'NONE',  ( 142.5447999999989861, -3659.504999999999654, 2272.030000000000200 ) ) ;
#3357=EDGE_CURVE ( 'NONE', #17996, #21912, #19296, .T. ) ;
#3371=CARTESIAN_POINT ( 'NONE',  ( 139.6999999999999886, -3579.494999999999891, 2272.030000000000200 ) ) ;
#3393=CARTESIAN_POINT ( 'NONE',  ( 137.2316813306051131, -3580.921433171091394, 2257.869726269903367 ) ) ;
#3414=FACE_OUTER_BOUND ( 'NONE', #8268, .T. ) ;
#3419=( NAMED_UNIT ( * ) PLANE_ANGLE_UNIT ( ) SI_UNIT ( $, .RADIAN. ) );
#3471=DIRECTION ( 'NONE',  ( 0.000000000000000000, -1.000000000000000000, 0.000000000000000000 ) ) ;
#3532=UNCERTAINTY_MEASURE_WITH_UNIT (LENGTH_MEASURE( 1.000000000000000082E-05 ), #4715, 'distance_accuracy_value', 'NONE');
#3790=AXIS2_PLACEMENT_3D ( 'NONE', #19009, #3062, #8814 ) ;
#3816=SHAPE_REPRESENTATION ( 'Roller 1', ( #5611 ), #9349 ) ;
#3953=AXIS2_PLACEMENT_3D ( 'NONE', #18002, #10855, #2299 ) ;
#4016=CARTESIAN_POINT ( 'NONE',  ( 137.8194210030732449, -3577.352480115512208, 2257.752117387002727 ) ) ;
#4107=CARTESIAN_POINT ( 'NONE',  ( 142.5447999999990998, -3659.693701068885275, 2257.962944264954785 ) ) ;
#4118=CARTESIAN_POINT ( 'NONE',  ( 137.8183059363161362, -3661.646540044306676, 2257.752309761470315 ) ) ;
#4129=ADVANCED_FACE ( 'NONE', ( #7267 ), #19694, .T. ) ;
#4243=CARTESIAN_POINT ( 'NONE',  ( 138.4364504168152621, -3576.939413531078117, 2257.663356991057299 ) ) ;
#4269=VERTEX_POINT ( 'NONE', #6093 ) ;
#4320=CARTESIAN_POINT ( 'NONE',  ( 142.5447999999989861, -3659.504999999999654, 2257.962944264955695 ) ) ;
#4389=CARTESIAN_POINT ( 'NONE',  ( 140.9635494321942417, -3582.050586540670338, 2257.663356974309863 ) ) ;
#4436=CARTESIAN_POINT ( 'NONE',  ( 141.1353819521796709, -3577.011135563875087, 2257.680384088092524 ) ) ;
#4484=EDGE_CURVE ( 'NONE', #21855, #10396, #19201, .T. ) ;
#4490=ORIENTED_EDGE ( 'NONE', *, *, #18998, .T. ) ;
#4497=CARTESIAN_POINT ( 'NONE',  ( 141.1265829755976711, -3581.963233858874901, 2257.683488260704507 ) ) ;
#4506=CARTESIAN_POINT ( 'NONE',  ( 136.9475605302572490, -3658.761901444864179, 2257.938841409468296 ) ) ;
#4534=DIRECTION ( 'NONE',  ( -1.000000000000000000, 0.000000000000000000, 0.000000000000000000 ) ) ;
#4539=CARTESIAN_POINT ( 'NONE',  ( 141.8426865358000271, -3657.624611564246152, 2257.800363195205136 ) ) ;
#4567=CARTESIAN_POINT ( 'NONE',  ( 139.6999999999999886, -3659.504999999999654, 2272.030000000000200 ) ) ;
#4573=CARTESIAN_POINT ( 'NONE',  ( 137.2316812770350225, -3660.931433079190356, 2257.869726282126976 ) ) ;
#4587=DIRECTION ( 'NONE',  ( 0.000000000000000000, 0.000000000000000000, -1.000000000000000000 ) ) ;
#4690=CARTESIAN_POINT ( 'NONE',  ( 138.7771837643548452, -3582.192323009303436, 2257.629692224586051 ) ) ;
#4715=( LENGTH_UNIT ( ) NAMED_UNIT ( * ) SI_UNIT ( .MILLI., .METRE. ) );
#4752=CARTESIAN_POINT ( 'NONE',  ( 139.6999999999999886, -3656.660200000000714, 2257.592639999999847 ) ) ;
#4886=ORIENTED_EDGE ( 'NONE', *, *, #404, .F. ) ;
#4893=CARTESIAN_POINT ( 'NONE',  ( 142.2556445798637412, -3658.241573636372777, 2257.890254707658642 ) ) ;
#5018=CARTESIAN_POINT ( 'NONE',  ( 142.3985385404256760, -3658.585513653864382, 2257.925021593836391 ) ) ;
#5215=CARTESIAN_POINT ( 'NONE',  ( 139.6999999999999886, -3570.287499999999909, 2257.592639999999847 ) ) ;
#5304=CARTESIAN_POINT ( 'NONE',  ( 137.9648833203323193, -3657.242990386724159, 2257.727830850464670 ) ) ;
#5486=VECTOR ( 'NONE', #21131, 1000.000000000000000 ) ;
#5611=AXIS2_PLACEMENT_3D ( 'NONE', #2606, #9751, #7545 ) ;
#5615=ORIENTED_EDGE ( 'NONE', *, *, #17292, .F. ) ;
#5675=ORIENTED_EDGE ( 'NONE', *, *, #7526, .F. ) ;
#5733=ORIENTED_EDGE ( 'NONE', *, *, #8969, .T. ) ;
#5818=EDGE_CURVE ( 'NONE', #18205, #17996, #22699, .T. ) ;
#5859=CYLINDRICAL_SURFACE ( 'NONE', #21433, 2.844799999999009010 ) ;
#5884=CARTESIAN_POINT ( 'NONE',  ( 141.9722846325389867, -3661.255981623820844, 2257.824198832787260 ) ) ;
#5923=EDGE_LOOP ( 'NONE', ( #18249, #13158 ) ) ;
#5935=CARTESIAN_POINT ( 'NONE',  ( 142.5262129393911152, -3579.870018574420101, 2257.957971591534715 ) ) ;
#6045=CARTESIAN_POINT ( 'NONE',  ( 139.6999999999999886, -3570.287499999999909, 2279.817639999999756 ) ) ;
#6093=CARTESIAN_POINT ( 'NONE',  ( 139.6999999999999886, -3582.339799999999286, 2257.592639999999847 ) ) ;
#6114=VERTEX_POINT ( 'NONE', #11110 ) ;
#6242=CARTESIAN_POINT ( 'NONE',  ( 139.6999999999999886, -3576.650200000000950, 2257.592639999999847 ) ) ;
#6275=CARTESIAN_POINT ( 'NONE',  ( 140.6195432067733577, -3582.193521822282946, 2257.629402108334489 ) ) ;
#6277=DIRECTION ( 'NONE',  ( 0.000000000000000000, -1.000000000000000000, 0.000000000000000000 ) ) ;
#6463=CARTESIAN_POINT ( 'NONE',  ( 137.9608668947936110, -3581.754029086221635, 2257.728452929456580 ) ) ;
#6515=CARTESIAN_POINT ( 'NONE',  ( 139.5113177728721610, -3656.660200000000714, 2257.592639999999847 ) ) ;
#6671=CARTESIAN_POINT ( 'NONE',  ( 142.4535506707765649, -3658.766509067717379, 2257.939127563549391 ) ) ;
#6747=CARTESIAN_POINT ( 'NONE',  ( 138.9614759198583727, -3656.751457182684589, 2257.615706725407563 ) ) ;
#6810=CARTESIAN_POINT ( 'NONE',  ( 137.1443557123595554, -3580.758427011661297, 2257.890254637431099 ) ) ;
#6835=DIRECTION ( 'NONE',  ( 1.000000000000000000, 0.000000000000000000, 0.000000000000000000 ) ) ;
#6860=CARTESIAN_POINT ( 'NONE',  ( 142.5447999999989861, -3659.504999999999654, 2257.962944264955695 ) ) ;
#6882=CIRCLE ( 'NONE', #18782, 11.11249999999999716 ) ;
#6958=VECTOR ( 'NONE', #2409, 1000.000000000000000 ) ;
#7030=DIRECTION ( 'NONE',  ( 1.000000000000000000, 0.000000000000000000, 0.000000000000000000 ) ) ;
#7267=FACE_OUTER_BOUND ( 'NONE', #16763, .T. ) ;
#7286=AXIS2_PLACEMENT_3D ( 'NONE', #13666, #1587, #10261 ) ;
#7311=ORIENTED_EDGE ( 'NONE', *, *, #17903, .T. ) ;
#7414=EDGE_CURVE ( 'NONE', #15102, #22318, #10457, .T. ) ;
#7447=DIRECTION ( 'NONE',  ( 1.000000000000000000, 0.000000000000000000, 0.000000000000000000 ) ) ;
#7526=EDGE_CURVE ( 'NONE', #14294, #21382, #22828, .T. ) ;
#7545=DIRECTION ( 'NONE',  ( 1.000000000000000000, 0.000000000000000000, 0.000000000000000000 ) ) ;
#7559=DIRECTION ( 'NONE',  ( 1.000000000000000000, 0.000000000000000000, 0.000000000000000000 ) ) ;
#7644=AXIS2_PLACEMENT_3D ( 'NONE', #10961, #14371, #7559 ) ;
#7699=APPLICATION_CONTEXT ( 'configuration controlled 3d designs of mechanical parts and assemblies' ) ;
#7758=CARTESIAN_POINT ( 'NONE',  ( 136.8737850040470505, -3659.879057353201461, 2257.957974146814649 ) ) ;
#7869=CARTESIAN_POINT ( 'NONE',  ( 136.8552000000009912, -3659.504999999999654, 2257.962944264955240 ) ) ;
#7875=CARTESIAN_POINT ( 'NONE',  ( 138.9614758940914214, -3576.741457189147241, 2257.615706727020552 ) ) ;
#8072=CARTESIAN_POINT ( 'NONE',  ( 139.6999999999999886, -3576.650200000000950, 2257.592639999999847 ) ) ;
#8085=CARTESIAN_POINT ( 'NONE',  ( 142.5447999999989861, -3659.504999999999654, 2257.962944264955695 ) ) ;
#8103=DIRECTION ( 'NONE',  ( 0.000000000000000000, -1.000000000000000000, 0.000000000000000000 ) ) ;
#8105=CARTESIAN_POINT ( 'NONE',  ( 136.8552000000009912, -3659.693686221675307, 2257.962944264956150 ) ) ;
#8141=ORIENTED_EDGE ( 'NONE', *, *, #9235, .T. ) ;
#8181=EDGE_LOOP ( 'NONE', ( #12059, #17886, #12343, #5615, #15936 ) ) ;
#8210=CARTESIAN_POINT ( 'NONE',  ( 137.8183059914243245, -3581.636540092137693, 2257.752309752018391 ) ) ;
#8268=EDGE_LOOP ( 'NONE', ( #2793, #17368 ) ) ;
#8399=DIRECTION ( 'NONE',  ( 0.000000000000000000, 0.000000000000000000, -1.000000000000000000 ) ) ;
#8440=ORIENTED_EDGE ( 'NONE', *, *, #4484, .T. ) ;
#8544=CARTESIAN_POINT ( 'NONE',  ( 140.0750197493808855, -3576.668786553544578, 2257.597441013394473 ) ) ;
#8566=CARTESIAN_POINT ( 'NONE',  ( 136.9464494900593934, -3580.233491490071174, 2257.939127522359740 ) ) ;
#8626=AXIS2_PLACEMENT_3D ( 'NONE', #22859, #22978, #6835 ) ;
#8791=SHAPE_DEFINITION_REPRESENTATION ( #19299, #3816 ) ;
#8814=DIRECTION ( 'NONE',  ( 0.000000000000000000, 0.000000000000000000, -1.000000000000000000 ) ) ;
#8874=EDGE_CURVE ( 'NONE', #10888, #2635, #1131, .T. ) ;
#8909=DIRECTION ( 'NONE',  ( 0.000000000000000000, -1.000000000000000000, 0.000000000000000000 ) ) ;
#8940=FACE_OUTER_BOUND ( 'NONE', #18793, .T. ) ;
#8969=EDGE_CURVE ( 'NONE', #22318, #4269, #20825, .T. ) ;
#9101=FACE_OUTER_BOUND ( 'NONE', #13166, .T. ) ;
#9181=EDGE_CURVE ( 'NONE', #18205, #10888, #20264, .T. ) ;
#9235=EDGE_CURVE ( 'NONE', #21912, #15765, #10486, .T. ) ;
#9297=EDGE_LOOP ( 'NONE', ( #1273, #10936 ) ) ;
#9349=( GEOMETRIC_REPRESENTATION_CONTEXT ( 3 ) GLOBAL_UNCERTAINTY_ASSIGNED_CONTEXT ( ( #3532 ) ) GLOBAL_UNIT_ASSIGNED_CONTEXT ( ( #4715, #19130, #20642 ) ) REPRESENTATION_CONTEXT ( 'NONE', 'WORKASPACE' ) );
#9408=CARTESIAN_POINT ( 'NONE',  ( 136.8552000000009912, -3579.306319665158753, 2257.962944264954785 ) ) ;
#9512=CARTESIAN_POINT ( 'NONE',  ( 136.9475604929545227, -3578.751901585129417, 2257.938841419043456 ) ) ;
#9588=DIRECTION ( 'NONE',  ( 0.000000000000000000, 1.000000000000000000, 0.000000000000000000 ) ) ;
#9623=CARTESIAN_POINT ( 'NONE',  ( 137.0014613743315408, -3660.424486175735638, 2257.925021614027628 ) ) ;
#9691=LINE ( 'NONE', #15203, #13316 ) ;
#9751=DIRECTION ( 'NONE',  ( 0.000000000000000000, 0.000000000000000000, 1.000000000000000000 ) ) ;
#9755=AXIS2_PLACEMENT_3D ( 'NONE', #16468, #18341, #14498 ) ;
#9767=CARTESIAN_POINT ( 'NONE',  ( 142.3973403485965719, -3580.417758129517097, 2257.924723937801900 ) ) ;
#9790=ADVANCED_FACE ( 'NONE', ( #8940 ), #16086, .F. ) ;
#9813=CARTESIAN_POINT ( 'NONE',  ( 136.8552000000009912, -3659.504999999999654, 2272.030000000000200 ) ) ;
#9819=DIRECTION ( 'NONE',  ( 0.000000000000000000, 0.000000000000000000, -1.000000000000000000 ) ) ;
#9838=CLOSED_SHELL ( 'NONE', ( #22646, #1994, #530, #18531, #1228, #384, #21728, #20898, #9790, #4129 ) ) ;
#9841=CARTESIAN_POINT ( 'NONE',  ( 139.6999999999999886, -3668.712499999999636, 2268.705139999999574 ) ) ;
#9856=AXIS2_PLACEMENT_3D ( 'NONE', #2683, #22242, #22137 ) ;
#9860=FACE_OUTER_BOUND ( 'NONE', #8181, .T. ) ;
#9926=CARTESIAN_POINT ( 'NONE',  ( 141.4511983580732704, -3657.232884635242499, 2257.728283137804738 ) ) ;
#10046=CARTESIAN_POINT ( 'NONE',  ( 142.5262150954257834, -3659.130943335864686, 2257.957974173014918 ) ) ;
#10056=CARTESIAN_POINT ( 'NONE',  ( 136.8552000000009912, -3659.504999999999654, 2257.962944264955240 ) ) ;
#10073=CARTESIAN_POINT ( 'NONE',  ( 139.3249801397857652, -3582.321213456867099, 2257.597441011073897 ) ) ;
#10171=PLANE ( 'NONE',  #14014 ) ;
#10193=CARTESIAN_POINT ( 'NONE',  ( 136.8552000000009912, -3579.494999999999891, 2257.962944264955695 ) ) ;
#10217=SHAPE_REPRESENTATION_RELATIONSHIP ( 'NONE' , 'NONE' ,  #3816, #12702 ) ;
#10261=DIRECTION ( 'NONE',  ( 1.000000000000000000, 0.000000000000000000, 0.000000000000000000 ) ) ;
#10293=DIRECTION ( 'NONE',  ( 0.000000000000000000, 0.000000000000000000, 1.000000000000000000 ) ) ;
#10396=VERTEX_POINT ( 'NONE', #1739 ) ;
#10408=CARTESIAN_POINT ( 'NONE',  ( 139.6999999999999886, -3659.504999999999654, 2272.030000000000200 ) ) ;
#10457=LINE ( 'NONE', #15275, #5486 ) ;
#10486=B_SPLINE_CURVE_WITH_KNOTS ( 'NONE', 3,
 ( #4320, #16960, #10046, #6671, #5018, #4893, #20835, #17419, #4539, #9926, #22577, #1022, #17074, #2781, #20952, #22700 ),
 .UNSPECIFIED., .F., .F.,
 ( 4, 2, 2, 2, 2, 2, 2, 4 ),
 ( 2.950257753427574957E-08, 0.0005578634888370243754, 0.001115697475096514343, 0.001673531461356004418, 0.002231365447615494494, 0.003347033420134704930, 0.003904867406394249216, 0.004462701392653794369 ),
 .UNSPECIFIED. ) ;
#10591=ORIENTED_EDGE ( 'NONE', *, *, #21943, .T. ) ;
#10623=DIRECTION ( 'NONE',  ( 0.000000000000000000, 0.000000000000000000, -1.000000000000000000 ) ) ;
#10855=DIRECTION ( 'NONE',  ( 0.000000000000000000, 0.000000000000000000, 1.000000000000000000 ) ) ;
#10888=VERTEX_POINT ( 'NONE', #10056 ) ;
#10936=ORIENTED_EDGE ( 'NONE', *, *, #1932, .T. ) ;
#10952=CARTESIAN_POINT ( 'NONE',  ( 139.6999999999999886, -3668.712499999999636, 2257.592639999999847 ) ) ;
#10961=CARTESIAN_POINT ( 'NONE',  ( 139.6999999999999886, -3579.494999999999891, 2272.030000000000200 ) ) ;
#10996=ORIENTED_EDGE ( 'NONE', *, *, #11707, .T. ) ;
#11072=DIRECTION ( 'NONE',  ( 0.000000000000000000, 0.000000000000000000, -1.000000000000000000 ) ) ;
#11110=CARTESIAN_POINT ( 'NONE',  ( 142.5447999999989861, -3579.494999999999891, 2272.030000000000200 ) ) ;
#11234=ORIENTED_EDGE ( 'NONE', *, *, #20515, .F. ) ;
#11264=CARTESIAN_POINT ( 'NONE',  ( 138.7771837325805393, -3662.202322998884483, 2257.629692227153555 ) ) ;
#11309=FACE_OUTER_BOUND ( 'NONE', #917, .T. ) ;
#11338=CARTESIAN_POINT ( 'NONE',  ( 139.6999999999999886, -3659.504999999999654, 2272.030000000000200 ) ) ;
#11362=CARTESIAN_POINT ( 'NONE',  ( 139.6999999999999886, -3662.349799999999050, 2257.592639999999847 ) ) ;
#11402=VECTOR ( 'NONE', #6277, 1000.000000000000000 ) ;
#11489=CARTESIAN_POINT ( 'NONE',  ( 139.6999999999999886, -3662.349799999999050, 2257.592639999999847 ) ) ;
#11523=B_SPLINE_CURVE_WITH_KNOTS ( 'NONE', 3,
 ( #6242, #20300, #12916, #7875, #497, #4243, #15027, #13252, #4016, #828, #20405, #15137, #9512, #18303, #9408, #2259 ),
 .UNSPECIFIED., .F., .F.,
 ( 4, 2, 2, 2, 2, 2, 2, 4 ),
 ( 0.008925572905118884029, 0.009483443516259321138, 0.01004131412739975825, 0.01059918473854019536, 0.01115705534968063073, 0.01227279657196156393, 0.01283066718310207563, 0.01338853779424258733 ),
 .UNSPECIFIED. ) ;
#11608=ORIENTED_EDGE ( 'NONE', *, *, #3357, .F. ) ;
#11631=CARTESIAN_POINT ( 'NONE',  ( 142.5447999999989861, -3579.683680193961209, 2257.962944264955695 ) ) ;
#11644=CARTESIAN_POINT ( 'NONE',  ( 136.8737869869528936, -3659.129981997597952, 2257.957971611072026 ) ) ;
#11707=EDGE_CURVE ( 'NONE', #4269, #21855, #3063, .T. ) ;
#11716=CARTESIAN_POINT ( 'NONE',  ( 137.4378580870267967, -3661.239941674269176, 2257.824813639031163 ) ) ;
#11764=CARTESIAN_POINT ( 'NONE',  ( 139.3259398483911013, -3656.678784355943208, 2257.597438744945066 ) ) ;
#11811=CARTESIAN_POINT ( 'NONE',  ( 142.5447999999989861, -3579.306313942341149, 2257.962944264954785 ) ) ;
#11840=ORIENTED_EDGE ( 'NONE', *, *, #18859, .F. ) ;
#11896=CARTESIAN_POINT ( 'NONE',  ( 136.8552000000010480, -3659.316319581317202, 2257.962944264956150 ) ) ;
#12007=CARTESIAN_POINT ( 'NONE',  ( 139.6999999999999886, -3570.287499999999909, 2257.592639999999847 ) ) ;
#12059=ORIENTED_EDGE ( 'NONE', *, *, #18998, .F. ) ;
#12063=EDGE_LOOP ( 'NONE', ( #17553, #18710, #4886, #18514, #16213 ) ) ;
#12112=CIRCLE ( 'NONE', #19598, 2.844799999999009010 ) ;
#12343=ORIENTED_EDGE ( 'NONE', *, *, #7414, .T. ) ;
#12380=ORIENTED_EDGE ( 'NONE', *, *, #17292, .T. ) ;
#12438=ORIENTED_EDGE ( 'NONE', *, *, #1932, .F. ) ;
#12447=CARTESIAN_POINT ( 'NONE',  ( 137.8194210580677463, -3657.362480067789875, 2257.752117377573541 ) ) ;
#12702=ADVANCED_BREP_SHAPE_REPRESENTATION ( '', ( #21472, #5611 ), #9349 ) ;
#12785=ORIENTED_EDGE ( 'NONE', *, *, #21741, .T. ) ;
#12887=CIRCLE ( 'NONE', #7644, 2.844799999999009010 ) ;
#12916=CARTESIAN_POINT ( 'NONE',  ( 139.3259398351677874, -3576.668784357255845, 2257.597438745286581 ) ) ;
#13021=CARTESIAN_POINT ( 'NONE',  ( 142.1839422283480872, -3660.940228195818236, 2257.872821505005959 ) ) ;
#13027=VECTOR ( 'NONE', #16743, 1000.000000000000000 ) ;
#13125=CARTESIAN_POINT ( 'NONE',  ( 140.6195432093131501, -3662.203521821452341, 2257.629402108538216 ) ) ;
#13153=ORIENTED_EDGE ( 'NONE', *, *, #8874, .T. ) ;
#13158=ORIENTED_EDGE ( 'NONE', *, *, #2787, .T. ) ;
#13166=EDGE_LOOP ( 'NONE', ( #14901, #4490, #14875, #1084, #2945 ) ) ;
#13182=CARTESIAN_POINT ( 'NONE',  ( 142.5447999999989861, -3579.494999999999891, 2257.962944264955695 ) ) ;
#13252=CARTESIAN_POINT ( 'NONE',  ( 137.9648832672151570, -3577.232990426899960, 2257.727830858807920 ) ) ;
#13316=VECTOR ( 'NONE', #13436, 1000.000000000000000 ) ;
#13355=CARTESIAN_POINT ( 'NONE',  ( 139.8886820246942193, -3662.349796521664302, 2257.592643472502914 ) ) ;
#13408=CARTESIAN_POINT ( 'NONE',  ( 139.6999999999999886, -3582.339799999999286, 2257.592639999999847 ) ) ;
#13436=DIRECTION ( 'NONE',  ( 0.000000000000000000, -1.000000000000000000, 0.000000000000000000 ) ) ;
#13443=FACE_OUTER_BOUND ( 'NONE', #12063, .T. ) ;
#13602=CARTESIAN_POINT ( 'NONE',  ( 138.2712681479159471, -3581.962087688927568, 2257.683753140937824 ) ) ;
#13666=CARTESIAN_POINT ( 'NONE',  ( 139.6999999999999886, -3668.712499999999636, 2268.705139999999574 ) ) ;
#13677=CARTESIAN_POINT ( 'NONE',  ( 139.6999999999999886, -3570.287499999999909, 2279.817639999999756 ) ) ;
#13777=CARTESIAN_POINT ( 'NONE',  ( 138.4364504584586655, -3656.949413510948489, 2257.663356986367944 ) ) ;
#13890=CARTESIAN_POINT ( 'NONE',  ( 138.7804567414061410, -3656.806478193061594, 2257.629402112182561 ) ) ;
#14002=LINE ( 'NONE', #5215, #20436 ) ;
#14014=AXIS2_PLACEMENT_3D ( 'NONE', #10408, #10293, #7030 ) ;
#14051=FACE_OUTER_BOUND ( 'NONE', #5923, .T. ) ;
#14071=CARTESIAN_POINT ( 'NONE',  ( 139.6999999999999886, -3570.287499999999909, 2268.705139999999574 ) ) ;
#14197=CARTESIAN_POINT ( 'NONE',  ( 136.8552000000009912, -3659.504999999999654, 2272.030000000000200 ) ) ;
#14294=VERTEX_POINT ( 'NONE', #12007 ) ;
#14318=FACE_OUTER_BOUND ( 'NONE', #9297, .T. ) ;
#14338=CARTESIAN_POINT ( 'NONE',  ( 139.6999999999999886, -3659.504999999999654, 2272.030000000000200 ) ) ;
#14371=DIRECTION ( 'NONE',  ( 0.000000000000000000, 0.000000000000000000, -1.000000000000000000 ) ) ;
#14415=CARTESIAN_POINT ( 'NONE',  ( 139.6999999999999886, -3582.339799999999286, 2257.592639999999847 ) ) ;
#14498=DIRECTION ( 'NONE',  ( -1.000000000000000000, 0.000000000000000000, 0.000000000000000000 ) ) ;
#14501=CARTESIAN_POINT ( 'NONE',  ( 139.6999999999999886, -3668.712499999999636, 2279.817639999999756 ) ) ;
#14612=LINE ( 'NONE', #16584, #6958 ) ;
#14790=CARTESIAN_POINT ( 'NONE',  ( 139.3249801263867482, -3662.331213455543548, 2257.597441011418596 ) ) ;
#14806=CARTESIAN_POINT ( 'NONE',  ( 139.6999999999999886, -3579.494999999999891, 2272.030000000000200 ) ) ;
#14836=CARTESIAN_POINT ( 'NONE',  ( 141.9722846279592261, -3581.245981629550442, 2257.824198831835020 ) ) ;
#14875=ORIENTED_EDGE ( 'NONE', *, *, #11707, .F. ) ;
#14881=EDGE_CURVE ( 'NONE', #15845, #22597, #6882, .T. ) ;
#14901=ORIENTED_EDGE ( 'NONE', *, *, #17903, .F. ) ;
#15027=CARTESIAN_POINT ( 'NONE',  ( 138.2734168420116134, -3577.026766243136080, 2257.683488283899806 ) ) ;
#15102=VERTEX_POINT ( 'NONE', #16958 ) ;
#15137=CARTESIAN_POINT ( 'NONE',  ( 137.0026594310930363, -3578.572242505815666, 2257.924723993070984 ) ) ;
#15170=CARTESIAN_POINT ( 'NONE',  ( 142.4524393039733354, -3580.238099177690401, 2257.938841366922134 ) ) ;
#15171=LINE ( 'NONE', #6045, #11402 ) ;
#15203=CARTESIAN_POINT ( 'NONE',  ( 139.6999999999999886, -3570.287499999999909, 2257.592639999999847 ) ) ;
#15241=CIRCLE ( 'NONE', #17469, 2.844799999999009010 ) ;
#15247=DIRECTION ( 'NONE',  ( 1.000000000000000000, 0.000000000000000000, 0.000000000000000000 ) ) ;
#15249=CARTESIAN_POINT ( 'NONE',  ( 137.1443556617770980, -3660.768426910471135, 2257.890254649414146 ) ) ;
#15275=CARTESIAN_POINT ( 'NONE',  ( 136.8552000000009912, -3579.494999999999891, 2272.030000000000200 ) ) ;
#15333=CARTESIAN_POINT ( 'NONE',  ( 142.3985385445537872, -3578.575513665826293, 2257.925021594871851 ) ) ;
#15708=CARTESIAN_POINT ( 'NONE',  ( 137.0014614162122655, -3580.414486297099756, 2257.925021603513869 ) ) ;
#15765=VERTEX_POINT ( 'NONE', #4752 ) ;
#15843=PLANE ( 'NONE',  #3790 ) ;
#15845=VERTEX_POINT ( 'NONE', #10952 ) ;
#15864=ORIENTED_EDGE ( 'NONE', *, *, #20139, .F. ) ;
#15936=ORIENTED_EDGE ( 'NONE', *, *, #4484, .F. ) ;
#16086=CYLINDRICAL_SURFACE ( 'NONE', #19345, 2.844799999999009010 ) ;
#16213=ORIENTED_EDGE ( 'NONE', *, *, #9181, .F. ) ;
#16243=CYLINDRICAL_SURFACE ( 'NONE', #9755, 2.844799999999009010 ) ;
#16282=CARTESIAN_POINT ( 'NONE',  ( 139.5113019466200228, -3582.339796537331949, 2257.592643468492042 ) ) ;
#16417=CARTESIAN_POINT ( 'NONE',  ( 139.6999999999999886, -3662.349799999999050, 2257.592639999999847 ) ) ;
#16468=CARTESIAN_POINT ( 'NONE',  ( 139.6999999999999886, -3579.494999999999891, 2272.030000000000200 ) ) ;
#16584=CARTESIAN_POINT ( 'NONE',  ( 139.6999999999999886, -3570.287499999999909, 2257.592639999999847 ) ) ;
#16741=UNCERTAINTY_MEASURE_WITH_UNIT (LENGTH_MEASURE( 1.000000000000000082E-05 ), #21126, 'distance_accuracy_value', 'NONE');
#16743=DIRECTION ( 'NONE',  ( 0.000000000000000000, 0.000000000000000000, -1.000000000000000000 ) ) ;
#16763=EDGE_LOOP ( 'NONE', ( #11234, #5675, #12785, #12380, #5733, #10591, #21697, #13153, #2222, #11840 ) ) ;
#16862=CARTESIAN_POINT ( 'NONE',  ( 142.3973403518663758, -3660.427758120067665, 2257.924723938623174 ) ) ;
#16911=AXIS2_PLACEMENT_3D ( 'NONE', #22222, #9588, #22005 ) ;
#16958=CARTESIAN_POINT ( 'NONE',  ( 136.8552000000009912, -3579.494999999999891, 2272.030000000000200 ) ) ;
#16960=CARTESIAN_POINT ( 'NONE',  ( 142.5447999999990998, -3659.316313936683400, 2257.962944264954331 ) ) ;
#16977=CARTESIAN_POINT ( 'NONE',  ( 141.5805787459278804, -3661.647520101402733, 2257.752117344049111 ) ) ;
#16983=DIRECTION ( 'NONE',  ( 1.000000000000000000, 0.000000000000000000, 0.000000000000000000 ) ) ;
#17074=CARTESIAN_POINT ( 'NONE',  ( 140.4431196388952401, -3656.752565539492480, 2257.615983594234422 ) ) ;
#17292=EDGE_CURVE ( 'NONE', #10396, #22318, #11523, .T. ) ;
#17333=CARTESIAN_POINT ( 'NONE',  ( 136.8737850351059535, -3579.869057567643722, 2257.957974138634654 ) ) ;
#17364=CIRCLE ( 'NONE', #7286, 11.11249999999999716 ) ;
#17368=ORIENTED_EDGE ( 'NONE', *, *, #18859, .T. ) ;
#17419=CARTESIAN_POINT ( 'NONE',  ( 141.9621417935377679, -3657.770058126337062, 2257.824813612040543 ) ) ;
#17464=AXIS2_PLACEMENT_3D ( 'NONE', #19322, #9819, #906 ) ;
#17469=AXIS2_PLACEMENT_3D ( 'NONE', #4567, #22484, #16983 ) ;
#17488=B_SPLINE_CURVE_WITH_KNOTS ( 'NONE', 3,
 ( #11362, #13355, #2353, #20385, #13125, #20499, #920, #18628, #16977, #5884, #13021, #16862, #2468, #20165, #4107, #8085 ),
 .UNSPECIFIED., .F., .F.,
 ( 4, 2, 2, 2, 2, 2, 2, 4 ),
 ( 0.01338840031623607721, 0.01394627866515972536, 0.01450415701408337178, 0.01506203536300701820, 0.01561991371193066636, 0.01673567040977796266, 0.01729354875870160735, 0.01785142710762525550 ),
 .UNSPECIFIED. ) ;
#17553=ORIENTED_EDGE ( 'NONE', *, *, #2787, .F. ) ;
#17627=ORIENTED_EDGE ( 'NONE', *, *, #14881, .F. ) ;
#17647=CYLINDRICAL_SURFACE ( 'NONE', #721, 11.11249999999985860 ) ;
#17849=ORIENTED_EDGE ( 'NONE', *, *, #5818, .F. ) ;
#17886=ORIENTED_EDGE ( 'NONE', *, *, #19022, .F. ) ;
#17891=CARTESIAN_POINT ( 'NONE',  ( 139.6999999999999886, -3570.287499999999909, 2268.705139999999574 ) ) ;
#17903=EDGE_CURVE ( 'NONE', #6114, #15102, #12112, .T. ) ;
#17996=VERTEX_POINT ( 'NONE', #3260 ) ;
#18002=CARTESIAN_POINT ( 'NONE',  ( 139.6999999999999886, -3579.494999999999891, 2272.030000000000200 ) ) ;
#18106=DIRECTION ( 'NONE',  ( 0.000000000000000000, 0.000000000000000000, -1.000000000000000000 ) ) ;
#18113=EDGE_CURVE ( 'NONE', #15765, #10888, #19044, .T. ) ;
#18205=VERTEX_POINT ( 'NONE', #14197 ) ;
#18249=ORIENTED_EDGE ( 'NONE', *, *, #5818, .T. ) ;
#18303=CARTESIAN_POINT ( 'NONE',  ( 136.8737869705807384, -3579.119982125134811, 2257.957971615415772 ) ) ;
#18333=AXIS2_PLACEMENT_3D ( 'NONE', #14071, #8909, #1634 ) ;
#18338=CARTESIAN_POINT ( 'NONE',  ( 141.4351164934280121, -3581.757009752985596, 2257.727830821389489 ) ) ;
#18341=DIRECTION ( 'NONE',  ( 0.000000000000000000, 0.000000000000000000, -1.000000000000000000 ) ) ;
#18411=CARTESIAN_POINT ( 'NONE',  ( 137.9608668417556032, -3661.764029045890766, 2257.728452937817110 ) ) ;
#18453=CARTESIAN_POINT ( 'NONE',  ( 139.8886820241594648, -3582.339796521665448, 2257.592643472502459 ) ) ;
#18460=PLANE ( 'NONE',  #3953 ) ;
#18514=ORIENTED_EDGE ( 'NONE', *, *, #8874, .F. ) ;
#18531=ADVANCED_FACE ( 'NONE', ( #14051 ), #10171, .F. ) ;
#18628=CARTESIAN_POINT ( 'NONE',  ( 141.4351164976492612, -3661.767009749791214, 2257.727830822052056 ) ) ;
#18629=ORIENTED_EDGE ( 'NONE', *, *, #9235, .F. ) ;
#18640=CARTESIAN_POINT ( 'NONE',  ( 138.9568794923274595, -3662.257434252253006, 2257.615983646263885 ) ) ;
#18710=ORIENTED_EDGE ( 'NONE', *, *, #3357, .T. ) ;
#18748=CARTESIAN_POINT ( 'NONE',  ( 136.9464494524225984, -3660.243491359982727, 2257.939127531997201 ) ) ;
#18782=AXIS2_PLACEMENT_3D ( 'NONE', #9841, #8103, #15247 ) ;
#18786=CIRCLE ( 'NONE', #16911, 11.11249999999999716 ) ;
#18789=CARTESIAN_POINT ( 'NONE',  ( 142.5447999999989861, -3579.494999999999891, 2257.962944264955695 ) ) ;
#18793=EDGE_LOOP ( 'NONE', ( #11608, #17849, #2900, #1820, #18629 ) ) ;
#18800=CARTESIAN_POINT ( 'NONE',  ( 136.8552000000009912, -3659.504999999999654, 2257.962944264955240 ) ) ;
#18859=EDGE_CURVE ( 'NONE', #22597, #15845, #17364, .T. ) ;
#18869=CARTESIAN_POINT ( 'NONE',  ( 137.5573135925616555, -3661.385388595491349, 2257.800363168595140 ) ) ;
#18922=CARTESIAN_POINT ( 'NONE',  ( 137.4277151414249829, -3657.754018655572963, 2257.824198879471169 ) ) ;
#18998=EDGE_CURVE ( 'NONE', #6114, #21855, #21634, .T. ) ;
#19009=CARTESIAN_POINT ( 'NONE',  ( 139.6999999999999886, -3668.712499999999636, 2268.705139999999574 ) ) ;
#19022=EDGE_CURVE ( 'NONE', #15102, #6114, #12887, .T. ) ;
#19044=B_SPLINE_CURVE_WITH_KNOTS ( 'NONE', 3,
 ( #22543, #6515, #11764, #6747, #13890, #13777, #21036, #5304, #12447, #18922, #20797, #19045, #4506, #11644, #11896, #18800 ),
 .UNSPECIFIED., .F., .F.,
 ( 4, 2, 2, 2, 2, 2, 2, 4 ),
 ( 0.004462701392653794369, 0.005020548996892072041, 0.005578396601130348846, 0.006136244205368626518, 0.006694091809606903323, 0.007809787018084332968, 0.008367634622322985341, 0.008925482226561637714 ),
 .UNSPECIFIED. ) ;
#19045=CARTESIAN_POINT ( 'NONE',  ( 137.0026594722382072, -3658.582242386909456, 2257.924723982745491 ) ) ;
#19130=( NAMED_UNIT ( * ) PLANE_ANGLE_UNIT ( ) SI_UNIT ( $, .RADIAN. ) );
#19199=CARTESIAN_POINT ( 'NONE',  ( 142.4535506740546964, -3578.756509080423257, 2257.939127564392948 ) ) ;
#19201=B_SPLINE_CURVE_WITH_KNOTS ( 'NONE', 3,
 ( #20714, #11811, #2909, #19199, #15333, #1140, #3138, #20595, #903, #22350, #4436, #20488, #1381, #8544, #22230, #8072 ),
 .UNSPECIFIED., .F., .F.,
 ( 4, 2, 2, 2, 2, 2, 2, 4 ),
 ( 0.004462717107651111709, 0.005020574082334379636, 0.005578431057017647562, 0.006136288031700915489, 0.006694145006384183416, 0.007809858955751593571, 0.008367715930435238800, 0.008925572905118884029 ),
 .UNSPECIFIED. ) ;
#19273=DIRECTION ( 'NONE',  ( 0.000000000000000000, -1.000000000000000000, 0.000000000000000000 ) ) ;
#19296=LINE ( 'NONE', #21292, #2494 ) ;
#19299=PRODUCT_DEFINITION_SHAPE ( 'NONE', 'NONE',  #22639 ) ;
#19322=CARTESIAN_POINT ( 'NONE',  ( 139.6999999999999886, -3659.504999999999654, 2272.030000000000200 ) ) ;
#19345=AXIS2_PLACEMENT_3D ( 'NONE', #14338, #36, #21482 ) ;
#19361=ORIENTED_EDGE ( 'NONE', *, *, #21943, .F. ) ;
#19598=AXIS2_PLACEMENT_3D ( 'NONE', #3371, #11072, #7447 ) ;
#19607=ORIENTED_EDGE ( 'NONE', *, *, #19022, .T. ) ;
#19694=CYLINDRICAL_SURFACE ( 'NONE', #18333, 11.11249999999985860 ) ;
#19776=FACE_OUTER_BOUND ( 'NONE', #21972, .T. ) ;
#20139=EDGE_CURVE ( 'NONE', #2635, #15845, #9691, .T. ) ;
#20165=CARTESIAN_POINT ( 'NONE',  ( 142.5262129412070067, -3659.880018561507768, 2257.957971592014019 ) ) ;
#20194=CYLINDRICAL_SURFACE ( 'NONE', #2804, 2.844799999999009010 ) ;
#20264=LINE ( 'NONE', #9813, #13027 ) ;
#20300=CARTESIAN_POINT ( 'NONE',  ( 139.5113177661436339, -3576.650200000001860, 2257.592639999999392 ) ) ;
#20385=CARTESIAN_POINT ( 'NONE',  ( 140.4385240681895084, -3662.258542810513973, 2257.615706727033739 ) ) ;
#20405=CARTESIAN_POINT ( 'NONE',  ( 137.2160574923763079, -3578.059772265523407, 2257.872821569613279 ) ) ;
#20436=VECTOR ( 'NONE', #19273, 1000.000000000000000 ) ;
#20440=CARTESIAN_POINT ( 'NONE',  ( 140.4385240661417527, -3582.248542811027164, 2257.615706726905501 ) ) ;
#20478=CARTESIAN_POINT ( 'NONE',  ( 136.8552000000009912, -3579.494999999999891, 2257.962944264955695 ) ) ;
#20488=CARTESIAN_POINT ( 'NONE',  ( 140.6228164711258728, -3576.797677065675089, 2257.629692243157024 ) ) ;
#20499=CARTESIAN_POINT ( 'NONE',  ( 140.9635494355036940, -3662.060586539072119, 2257.663356974682301 ) ) ;
#20515=EDGE_CURVE ( 'NONE', #21382, #22597, #15171, .T. ) ;
#20540=ORIENTED_EDGE ( 'NONE', *, *, #20515, .T. ) ;
#20583=DIRECTION ( 'NONE',  ( 0.000000000000000000, 0.000000000000000000, -1.000000000000000000 ) ) ;
#20595=CARTESIAN_POINT ( 'NONE',  ( 141.9621417992156864, -3577.760058133676011, 2257.824813613222886 ) ) ;
#20642=( NAMED_UNIT ( * ) SI_UNIT ( $, .STERADIAN. ) SOLID_ANGLE_UNIT ( ) );
#20714=CARTESIAN_POINT ( 'NONE',  ( 142.5447999999989861, -3579.494999999999891, 2257.962944264955695 ) ) ;
#20742=CARTESIAN_POINT ( 'NONE',  ( 138.4354735775639256, -3582.050017445782032, 2257.663486765196467 ) ) ;
#20797=CARTESIAN_POINT ( 'NONE',  ( 137.2160575470620927, -3658.069772174391346, 2257.872821556948566 ) ) ;
#20825=B_SPLINE_CURVE_WITH_KNOTS ( 'NONE', 3,
 ( #10193, #20981, #17333, #8566, #15708, #6810, #3393, #1055, #22489, #8210, #6463, #13602, #20742, #4690, #2936, #10073, #16282, #14415 ),
 .UNSPECIFIED., .F., .F.,
 ( 4, 2, 2, 2, 2, 2, 2, 2, 4 ),
 ( 0.01338853779424258733, 0.01394642552155045574, 0.01450431324885832415, 0.01506220097616619430, 0.01562008870347406271, 0.01617797643078193112, 0.01673586415808980127, 0.01729375188539766794, 0.01785163961270553809 ),
 .UNSPECIFIED. ) ;
#20835=CARTESIAN_POINT ( 'NONE',  ( 142.1683190381772590, -3658.078567413148448, 2257.869726351763802 ) ) ;
#20898=ADVANCED_FACE ( 'NONE', ( #9860 ), #20194, .F. ) ;
#20952=CARTESIAN_POINT ( 'NONE',  ( 139.8886776210838434, -3656.660200000000714, 2257.592639999999392 ) ) ;
#20975=PRODUCT ( 'Roller 1', 'Roller 1', '', ( #22260 ) ) ;
#20981=CARTESIAN_POINT ( 'NONE',  ( 136.8552000000009627, -3579.683686123789812, 2257.962944264955240 ) ) ;
#21036=CARTESIAN_POINT ( 'NONE',  ( 138.2734168879149195, -3657.036766217124296, 2257.683488278010373 ) ) ;
#21126=( LENGTH_UNIT ( ) NAMED_UNIT ( * ) SI_UNIT ( .MILLI., .METRE. ) );
#21131=DIRECTION ( 'NONE',  ( 0.000000000000000000, 0.000000000000000000, -1.000000000000000000 ) ) ;
#21292=CARTESIAN_POINT ( 'NONE',  ( 142.5447999999989861, -3659.504999999999654, 2272.030000000000200 ) ) ;
#21382=VERTEX_POINT ( 'NONE', #13677 ) ;
#21433=AXIS2_PLACEMENT_3D ( 'NONE', #11338, #20583, #4534 ) ;
#21472=MANIFOLD_SOLID_BREP ( 'SOLID2-14[1]', #9838 ) ;
#21482=DIRECTION ( 'NONE',  ( -1.000000000000000000, 0.000000000000000000, 0.000000000000000000 ) ) ;
#21634=LINE ( 'NONE', #1708, #22975 ) ;
#21697=ORIENTED_EDGE ( 'NONE', *, *, #18113, .T. ) ;
#21728=ADVANCED_FACE ( 'NONE', ( #11309 ), #18460, .F. ) ;
#21741=EDGE_CURVE ( 'NONE', #14294, #10396, #14612, .T. ) ;
#21855=VERTEX_POINT ( 'NONE', #13182 ) ;
#21912=VERTEX_POINT ( 'NONE', #6860 ) ;
#21928=CARTESIAN_POINT ( 'NONE',  ( 139.5113228070520393, -3662.349796537330803, 2257.592643468492952 ) ) ;
#21943=EDGE_CURVE ( 'NONE', #4269, #15765, #14002, .T. ) ;
#21972=EDGE_LOOP ( 'NONE', ( #12438, #20540, #17627, #15864, #3011, #8141, #19361, #10996, #8440, #107 ) ) ;
#22005=DIRECTION ( 'NONE',  ( 1.000000000000000000, 0.000000000000000000, 0.000000000000000000 ) ) ;
#22137=DIRECTION ( 'NONE',  ( 0.000000000000000000, 0.000000000000000000, -1.000000000000000000 ) ) ;
#22148=CARTESIAN_POINT ( 'NONE',  ( 138.4354735356341735, -3662.060017425506430, 2257.663486769918109 ) ) ;
#22222=CARTESIAN_POINT ( 'NONE',  ( 139.6999999999999886, -3570.287499999999909, 2268.705139999999574 ) ) ;
#22230=CARTESIAN_POINT ( 'NONE',  ( 139.8886776217523220, -3576.650200000001405, 2257.592640000000301 ) ) ;
#22242=DIRECTION ( 'NONE',  ( 0.000000000000000000, -1.000000000000000000, 0.000000000000000000 ) ) ;
#22260=PRODUCT_CONTEXT ( 'NONE', #1993, 'mechanical' ) ;
#22318=VERTEX_POINT ( 'NONE', #20478 ) ;
#22350=CARTESIAN_POINT ( 'NONE',  ( 141.4511983633885279, -3577.222884639119002, 2257.728283138646020 ) ) ;
#22484=DIRECTION ( 'NONE',  ( 0.000000000000000000, 0.000000000000000000, -1.000000000000000000 ) ) ;
#22489=CARTESIAN_POINT ( 'NONE',  ( 137.5573136500408395, -3581.375388660315821, 2257.800363157316951 ) ) ;
#22543=CARTESIAN_POINT ( 'NONE',  ( 139.6999999999999886, -3656.660200000000714, 2257.592639999999847 ) ) ;
#22577=CARTESIAN_POINT ( 'NONE',  ( 141.1353819475458522, -3657.021135561388746, 2257.680384087519542 ) ) ;
#22597=VERTEX_POINT ( 'NONE', #14501 ) ;
#22639=PRODUCT_DEFINITION ( 'UNKNOWN', '', #741, #2927 ) ;
#22646=ADVANCED_FACE ( 'NONE', ( #19776 ), #17647, .T. ) ;
#22699=CIRCLE ( 'NONE', #17464, 2.844799999999009010 ) ;
#22700=CARTESIAN_POINT ( 'NONE',  ( 139.6999999999999886, -3656.660200000000714, 2257.592639999999847 ) ) ;
#22828=CIRCLE ( 'NONE', #8626, 11.11249999999999716 ) ;
#22859=CARTESIAN_POINT ( 'NONE',  ( 139.6999999999999886, -3570.287499999999909, 2268.705139999999574 ) ) ;
#22975=VECTOR ( 'NONE', #18106, 1000.000000000000000 ) ;
#22978=DIRECTION ( 'NONE',  ( 0.000000000000000000, 1.000000000000000000, 0.000000000000000000 ) ) ;
#23094=( NAMED_UNIT ( * ) SI_UNIT ( $, .STERADIAN. ) SOLID_ANGLE_UNIT ( ) );
#23187=COLOUR_RGB('Light Blue',0.38,0.62,0.78);
#23188=FILL_AREA_STYLE_COLOUR('',#23187);
#23189=FILL_AREA_STYLE('',(#23188));
#23190=SURFACE_STYLE_FILL_AREA(#23189);
#23191=SURFACE_SIDE_STYLE('',(#23190));
#23192=SURFACE_STYLE_USAGE(.BOTH.,#23191);
#23193=PRESENTATION_STYLE_ASSIGNMENT((#23192));
#23226=STYLED_ITEM('',(#23193),#21472);
#23237=MECHANICAL_DESIGN_GEOMETRIC_PRESENTATION_REPRESENTATION('',(#23226),#2257);
ENDSEC;
END-ISO-10303-21;
